ISO-10303-21;
HEADER;
/* Generated by software containing ST-Developer
 * from STEP Tools, Inc. (www.steptools.com) 
 */

FILE_DESCRIPTION(
/* description */ ('PAT-054'),
/* implementation_level */ '2;1');

FILE_NAME(
/* name */ 'Cap Screw - M5x20.step',
/* time_stamp */ '2026-10-29T16:38:13-07:00',
/* author */ (''),
/* organization */ (''),
/* preprocessor_version */ 'ST-DEVELOPER v20.2',
/* originating_system */ 'Autodesk Translation Framework v15.17.0.0',
/* authorisation */ '');

FILE_SCHEMA (('AUTOMOTIVE_DESIGN { 1 0 10303 214 3 1 1 }'));
ENDSEC;

DATA;
#10=MECHANICAL_DESIGN_GEOMETRIC_PRESENTATION_REPRESENTATION('',(#947),#33981);
#18=ORIENTED_CLOSED_SHELL('',*,#13062,.F.);
#23=BREP_WITH_VOIDS('Body1',#13061,(#18));
#797=CONICAL_SURFACE('',#14502,0.4,0.785398163397448);
#798=CONICAL_SURFACE('',#14506,0.41,0.785398163397448);
#799=CONICAL_SURFACE('',#14510,0.26,0.463647609000806);
#800=CONICAL_SURFACE('',#14514,0.225,0.785398163397448);
#844=SHAPE_REPRESENTATION_RELATIONSHIP('SRR','None',#34221,#888);
#888=ADVANCED_BREP_SHAPE_REPRESENTATION('',(#23),#33969);
#947=STYLED_ITEM('',(#34524),#23);
#1203=FACE_BOUND('',#2982,.T.);
#1504=PLANE('',#14500);
#1505=PLANE('',#14508);
#1506=PLANE('',#14516);
#1507=PLANE('',#14517);
#1508=PLANE('',#14518);
#1509=PLANE('',#14519);
#1510=PLANE('',#14520);
#1511=PLANE('',#14521);
#1512=PLANE('',#14522);
#1513=PLANE('',#14523);
#1514=PLANE('',#14524);
#2063=FACE_OUTER_BOUND('',#2977,.T.);
#2064=FACE_OUTER_BOUND('',#2978,.T.);
#2065=FACE_OUTER_BOUND('',#2979,.T.);
#2066=FACE_OUTER_BOUND('',#2980,.T.);
#2067=FACE_OUTER_BOUND('',#2981,.T.);
#2068=FACE_OUTER_BOUND('',#2983,.T.);
#2069=FACE_OUTER_BOUND('',#2984,.T.);
#2070=FACE_OUTER_BOUND('',#2985,.T.);
#2071=FACE_OUTER_BOUND('',#2986,.T.);
#2072=FACE_OUTER_BOUND('',#2987,.T.);
#2073=FACE_OUTER_BOUND('',#2988,.T.);
#2074=FACE_OUTER_BOUND('',#2989,.T.);
#2075=FACE_OUTER_BOUND('',#2990,.T.);
#2076=FACE_OUTER_BOUND('',#2991,.T.);
#2077=FACE_OUTER_BOUND('',#2992,.T.);
#2078=FACE_OUTER_BOUND('',#2993,.T.);
#2079=FACE_OUTER_BOUND('',#2994,.T.);
#2977=EDGE_LOOP('',(#10783));
#2978=EDGE_LOOP('',(#10784,#10785,#10786,#10787));
#2979=EDGE_LOOP('',(#10788,#10789,#10790,#10791));
#2980=EDGE_LOOP('',(#10792,#10793,#10794,#10795));
#2981=EDGE_LOOP('',(#10796));
#2982=EDGE_LOOP('',(#10797));
#2983=EDGE_LOOP('',(#10798,#10799,#10800,#10801));
#2984=EDGE_LOOP('',(#10802,#10803,#10804,#10805));
#2985=EDGE_LOOP('',(#10806,#10807,#10808,#10809));
#2986=EDGE_LOOP('',(#10810));
#2987=EDGE_LOOP('',(#10811,#10812,#10813,#10814));
#2988=EDGE_LOOP('',(#10815,#10816,#10817,#10818));
#2989=EDGE_LOOP('',(#10819,#10820,#10821,#10822));
#2990=EDGE_LOOP('',(#10823,#10824,#10825,#10826));
#2991=EDGE_LOOP('',(#10827,#10828,#10829,#10830));
#2992=EDGE_LOOP('',(#10831,#10832,#10833,#10834));
#2993=EDGE_LOOP('',(#10835,#10836,#10837,#10838,#10839,#10840));
#2994=EDGE_LOOP('',(#10841,#10842,#10843,#10844,#10845,#10846));
#3907=LINE('',#23619,#4841);
#3908=LINE('',#23623,#4842);
#3909=LINE('',#23627,#4843);
#3910=LINE('',#23634,#4844);
#3911=LINE('',#23638,#4845);
#3912=LINE('',#23642,#4846);
#3913=LINE('',#23647,#4847);
#3914=LINE('',#23649,#4848);
#3915=LINE('',#23651,#4849);
#3916=LINE('',#23652,#4850);
#3917=LINE('',#23655,#4851);
#3918=LINE('',#23657,#4852);
#3919=LINE('',#23658,#4853);
#3920=LINE('',#23661,#4854);
#3921=LINE('',#23663,#4855);
#3922=LINE('',#23664,#4856);
#3923=LINE('',#23667,#4857);
#3924=LINE('',#23669,#4858);
#3925=LINE('',#23670,#4859);
#3926=LINE('',#23673,#4860);
#3927=LINE('',#23675,#4861);
#3928=LINE('',#23676,#4862);
#3929=LINE('',#23678,#4863);
#3930=LINE('',#23679,#4864);
#4841=VECTOR('',#17450,0.4);
#4842=VECTOR('',#17455,0.425);
#4843=VECTOR('',#17460,0.41);
#4844=VECTOR('',#17469,0.26);
#4845=VECTOR('',#17474,0.25);
#4846=VECTOR('',#17479,0.225);
#4847=VECTOR('',#17484,1.);
#4848=VECTOR('',#17485,1.);
#4849=VECTOR('',#17486,1.);
#4850=VECTOR('',#17487,1.);
#4851=VECTOR('',#17490,1.);
#4852=VECTOR('',#17491,1.);
#4853=VECTOR('',#17492,1.);
#4854=VECTOR('',#17495,1.);
#4855=VECTOR('',#17496,1.);
#4856=VECTOR('',#17497,1.);
#4857=VECTOR('',#17500,1.);
#4858=VECTOR('',#17501,1.);
#4859=VECTOR('',#17502,1.);
#4860=VECTOR('',#17505,1.);
#4861=VECTOR('',#17506,1.);
#4862=VECTOR('',#17507,1.);
#4863=VECTOR('',#17510,1.);
#4864=VECTOR('',#17511,1.);
#5505=CIRCLE('',#14501,0.375);
#5506=CIRCLE('',#14503,0.425);
#5507=CIRCLE('',#14505,0.425);
#5508=CIRCLE('',#14507,0.395);
#5509=CIRCLE('',#14509,0.27);
#5510=CIRCLE('',#14511,0.24505);
#5511=CIRCLE('',#14513,0.24505);
#5512=CIRCLE('',#14515,0.2);
#6348=VERTEX_POINT('',#23614);
#6349=VERTEX_POINT('',#23617);
#6350=VERTEX_POINT('',#23621);
#6351=VERTEX_POINT('',#23625);
#6352=VERTEX_POINT('',#23629);
#6353=VERTEX_POINT('',#23632);
#6354=VERTEX_POINT('',#23636);
#6355=VERTEX_POINT('',#23640);
#6356=VERTEX_POINT('',#23645);
#6357=VERTEX_POINT('',#23646);
#6358=VERTEX_POINT('',#23648);
#6359=VERTEX_POINT('',#23650);
#6360=VERTEX_POINT('',#23654);
#6361=VERTEX_POINT('',#23656);
#6362=VERTEX_POINT('',#23660);
#6363=VERTEX_POINT('',#23662);
#6364=VERTEX_POINT('',#23666);
#6365=VERTEX_POINT('',#23668);
#6366=VERTEX_POINT('',#23672);
#6367=VERTEX_POINT('',#23674);
#7891=EDGE_CURVE('',#6348,#6348,#5505,.T.);
#7892=EDGE_CURVE('',#6349,#6349,#5506,.T.);
#7893=EDGE_CURVE('',#6349,#6348,#3907,.T.);
#7894=EDGE_CURVE('',#6350,#6350,#5507,.T.);
#7895=EDGE_CURVE('',#6350,#6349,#3908,.T.);
#7896=EDGE_CURVE('',#6351,#6351,#5508,.T.);
#7897=EDGE_CURVE('',#6351,#6350,#3909,.T.);
#7898=EDGE_CURVE('',#6352,#6352,#5509,.T.);
#7899=EDGE_CURVE('',#6353,#6353,#5510,.F.);
#7900=EDGE_CURVE('',#6353,#6352,#3910,.T.);
#7901=EDGE_CURVE('',#6354,#6354,#5511,.F.);
#7902=EDGE_CURVE('',#6354,#6353,#3911,.T.);
#7903=EDGE_CURVE('',#6355,#6355,#5512,.T.);
#7904=EDGE_CURVE('',#6355,#6354,#3912,.T.);
#7905=EDGE_CURVE('',#6356,#6357,#3913,.T.);
#7906=EDGE_CURVE('',#6357,#6358,#3914,.T.);
#7907=EDGE_CURVE('',#6358,#6359,#3915,.T.);
#7908=EDGE_CURVE('',#6356,#6359,#3916,.T.);
#7909=EDGE_CURVE('',#6357,#6360,#3917,.T.);
#7910=EDGE_CURVE('',#6360,#6361,#3918,.T.);
#7911=EDGE_CURVE('',#6361,#6358,#3919,.T.);
#7912=EDGE_CURVE('',#6360,#6362,#3920,.T.);
#7913=EDGE_CURVE('',#6362,#6363,#3921,.T.);
#7914=EDGE_CURVE('',#6363,#6361,#3922,.T.);
#7915=EDGE_CURVE('',#6362,#6364,#3923,.T.);
#7916=EDGE_CURVE('',#6364,#6365,#3924,.T.);
#7917=EDGE_CURVE('',#6365,#6363,#3925,.T.);
#7918=EDGE_CURVE('',#6364,#6366,#3926,.T.);
#7919=EDGE_CURVE('',#6366,#6367,#3927,.T.);
#7920=EDGE_CURVE('',#6367,#6365,#3928,.T.);
#7921=EDGE_CURVE('',#6366,#6356,#3929,.T.);
#7922=EDGE_CURVE('',#6359,#6367,#3930,.T.);
#10783=ORIENTED_EDGE('',*,*,#7891,.F.);
#10784=ORIENTED_EDGE('',*,*,#7892,.F.);
#10785=ORIENTED_EDGE('',*,*,#7893,.T.);
#10786=ORIENTED_EDGE('',*,*,#7891,.T.);
#10787=ORIENTED_EDGE('',*,*,#7893,.F.);
#10788=ORIENTED_EDGE('',*,*,#7894,.F.);
#10789=ORIENTED_EDGE('',*,*,#7895,.T.);
#10790=ORIENTED_EDGE('',*,*,#7892,.T.);
#10791=ORIENTED_EDGE('',*,*,#7895,.F.);
#10792=ORIENTED_EDGE('',*,*,#7896,.F.);
#10793=ORIENTED_EDGE('',*,*,#7897,.T.);
#10794=ORIENTED_EDGE('',*,*,#7894,.T.);
#10795=ORIENTED_EDGE('',*,*,#7897,.F.);
#10796=ORIENTED_EDGE('',*,*,#7896,.T.);
#10797=ORIENTED_EDGE('',*,*,#7898,.F.);
#10798=ORIENTED_EDGE('',*,*,#7899,.F.);
#10799=ORIENTED_EDGE('',*,*,#7900,.T.);
#10800=ORIENTED_EDGE('',*,*,#7898,.T.);
#10801=ORIENTED_EDGE('',*,*,#7900,.F.);
#10802=ORIENTED_EDGE('',*,*,#7901,.F.);
#10803=ORIENTED_EDGE('',*,*,#7902,.T.);
#10804=ORIENTED_EDGE('',*,*,#7899,.T.);
#10805=ORIENTED_EDGE('',*,*,#7902,.F.);
#10806=ORIENTED_EDGE('',*,*,#7903,.F.);
#10807=ORIENTED_EDGE('',*,*,#7904,.T.);
#10808=ORIENTED_EDGE('',*,*,#7901,.T.);
#10809=ORIENTED_EDGE('',*,*,#7904,.F.);
#10810=ORIENTED_EDGE('',*,*,#7903,.T.);
#10811=ORIENTED_EDGE('',*,*,#7905,.T.);
#10812=ORIENTED_EDGE('',*,*,#7906,.T.);
#10813=ORIENTED_EDGE('',*,*,#7907,.T.);
#10814=ORIENTED_EDGE('',*,*,#7908,.F.);
#10815=ORIENTED_EDGE('',*,*,#7909,.T.);
#10816=ORIENTED_EDGE('',*,*,#7910,.T.);
#10817=ORIENTED_EDGE('',*,*,#7911,.T.);
#10818=ORIENTED_EDGE('',*,*,#7906,.F.);
#10819=ORIENTED_EDGE('',*,*,#7912,.T.);
#10820=ORIENTED_EDGE('',*,*,#7913,.T.);
#10821=ORIENTED_EDGE('',*,*,#7914,.T.);
#10822=ORIENTED_EDGE('',*,*,#7910,.F.);
#10823=ORIENTED_EDGE('',*,*,#7915,.T.);
#10824=ORIENTED_EDGE('',*,*,#7916,.T.);
#10825=ORIENTED_EDGE('',*,*,#7917,.T.);
#10826=ORIENTED_EDGE('',*,*,#7913,.F.);
#10827=ORIENTED_EDGE('',*,*,#7918,.T.);
#10828=ORIENTED_EDGE('',*,*,#7919,.T.);
#10829=ORIENTED_EDGE('',*,*,#7920,.T.);
#10830=ORIENTED_EDGE('',*,*,#7916,.F.);
#10831=ORIENTED_EDGE('',*,*,#7921,.T.);
#10832=ORIENTED_EDGE('',*,*,#7908,.T.);
#10833=ORIENTED_EDGE('',*,*,#7922,.T.);
#10834=ORIENTED_EDGE('',*,*,#7919,.F.);
#10835=ORIENTED_EDGE('',*,*,#7921,.F.);
#10836=ORIENTED_EDGE('',*,*,#7918,.F.);
#10837=ORIENTED_EDGE('',*,*,#7915,.F.);
#10838=ORIENTED_EDGE('',*,*,#7912,.F.);
#10839=ORIENTED_EDGE('',*,*,#7909,.F.);
#10840=ORIENTED_EDGE('',*,*,#7905,.F.);
#10841=ORIENTED_EDGE('',*,*,#7922,.F.);
#10842=ORIENTED_EDGE('',*,*,#7907,.F.);
#10843=ORIENTED_EDGE('',*,*,#7911,.F.);
#10844=ORIENTED_EDGE('',*,*,#7914,.F.);
#10845=ORIENTED_EDGE('',*,*,#7917,.F.);
#10846=ORIENTED_EDGE('',*,*,#7920,.F.);
#12135=CYLINDRICAL_SURFACE('',#14504,0.425);
#12136=CYLINDRICAL_SURFACE('',#14512,0.24505);
#12775=ADVANCED_FACE('',(#2063),#1504,.T.);
#12776=ADVANCED_FACE('',(#2064),#797,.T.);
#12777=ADVANCED_FACE('',(#2065),#12135,.T.);
#12778=ADVANCED_FACE('',(#2066),#798,.T.);
#12779=ADVANCED_FACE('',(#2067,#1203),#1505,.T.);
#12780=ADVANCED_FACE('',(#2068),#799,.T.);
#12781=ADVANCED_FACE('',(#2069),#12136,.T.);
#12782=ADVANCED_FACE('',(#2070),#800,.T.);
#12783=ADVANCED_FACE('',(#2071),#1506,.T.);
#12784=ADVANCED_FACE('',(#2072),#1507,.F.);
#12785=ADVANCED_FACE('',(#2073),#1508,.F.);
#12786=ADVANCED_FACE('',(#2074),#1509,.F.);
#12787=ADVANCED_FACE('',(#2075),#1510,.F.);
#12788=ADVANCED_FACE('',(#2076),#1511,.F.);
#12789=ADVANCED_FACE('',(#2077),#1512,.F.);
#12790=ADVANCED_FACE('',(#2078),#1513,.F.);
#12791=ADVANCED_FACE('',(#2079),#1514,.F.);
#13061=CLOSED_SHELL('',(#12775,#12776,#12777,#12778,#12779,#12780,#12781,
#12782,#12783));
#13062=CLOSED_SHELL('',(#12784,#12785,#12786,#12787,#12788,#12789,#12790,
#12791));
#14499=AXIS2_PLACEMENT_3D('',#23612,#17440,#17441);
#14500=AXIS2_PLACEMENT_3D('',#23613,#17442,#17443);
#14501=AXIS2_PLACEMENT_3D('',#23615,#17444,#17445);
#14502=AXIS2_PLACEMENT_3D('',#23616,#17446,#17447);
#14503=AXIS2_PLACEMENT_3D('',#23618,#17448,#17449);
#14504=AXIS2_PLACEMENT_3D('',#23620,#17451,#17452);
#14505=AXIS2_PLACEMENT_3D('',#23622,#17453,#17454);
#14506=AXIS2_PLACEMENT_3D('',#23624,#17456,#17457);
#14507=AXIS2_PLACEMENT_3D('',#23626,#17458,#17459);
#14508=AXIS2_PLACEMENT_3D('',#23628,#17461,#17462);
#14509=AXIS2_PLACEMENT_3D('',#23630,#17463,#17464);
#14510=AXIS2_PLACEMENT_3D('',#23631,#17465,#17466);
#14511=AXIS2_PLACEMENT_3D('',#23633,#17467,#17468);
#14512=AXIS2_PLACEMENT_3D('',#23635,#17470,#17471);
#14513=AXIS2_PLACEMENT_3D('',#23637,#17472,#17473);
#14514=AXIS2_PLACEMENT_3D('',#23639,#17475,#17476);
#14515=AXIS2_PLACEMENT_3D('',#23641,#17477,#17478);
#14516=AXIS2_PLACEMENT_3D('',#23643,#17480,#17481);
#14517=AXIS2_PLACEMENT_3D('',#23644,#17482,#17483);
#14518=AXIS2_PLACEMENT_3D('',#23653,#17488,#17489);
#14519=AXIS2_PLACEMENT_3D('',#23659,#17493,#17494);
#14520=AXIS2_PLACEMENT_3D('',#23665,#17498,#17499);
#14521=AXIS2_PLACEMENT_3D('',#23671,#17503,#17504);
#14522=AXIS2_PLACEMENT_3D('',#23677,#17508,#17509);
#14523=AXIS2_PLACEMENT_3D('',#23680,#17512,#17513);
#14524=AXIS2_PLACEMENT_3D('',#23681,#17514,#17515);
#17440=DIRECTION('axis',(0.,0.,1.));
#17441=DIRECTION('refdir',(1.,0.,0.));
#17442=DIRECTION('center_axis',(0.,1.,0.));
#17443=DIRECTION('ref_axis',(0.,0.,1.));
#17444=DIRECTION('center_axis',(0.,-1.,0.));
#17445=DIRECTION('ref_axis',(1.,0.,0.));
#17446=DIRECTION('center_axis',(0.,-1.,0.));
#17447=DIRECTION('ref_axis',(1.,0.,0.));
#17448=DIRECTION('center_axis',(0.,-1.,0.));
#17449=DIRECTION('ref_axis',(1.,0.,0.));
#17450=DIRECTION('',(0.707106781186548,0.707106781186547,8.65956056235493E-17));
#17451=DIRECTION('center_axis',(0.,-1.,0.));
#17452=DIRECTION('ref_axis',(1.,0.,0.));
#17453=DIRECTION('center_axis',(0.,-1.,0.));
#17454=DIRECTION('ref_axis',(1.,0.,0.));
#17455=DIRECTION('',(0.,1.,0.));
#17456=DIRECTION('center_axis',(0.,1.,0.));
#17457=DIRECTION('ref_axis',(1.,0.,0.));
#17458=DIRECTION('center_axis',(0.,-1.,0.));
#17459=DIRECTION('ref_axis',(1.,0.,0.));
#17460=DIRECTION('',(-0.707106781186547,0.707106781186548,-8.65956056235493E-17));
#17461=DIRECTION('center_axis',(0.,-1.,0.));
#17462=DIRECTION('ref_axis',(0.,0.,-1.));
#17463=DIRECTION('center_axis',(0.,-1.,0.));
#17464=DIRECTION('ref_axis',(1.,0.,0.));
#17465=DIRECTION('center_axis',(0.,1.,0.));
#17466=DIRECTION('ref_axis',(1.,0.,0.));
#17467=DIRECTION('center_axis',(0.,1.,0.));
#17468=DIRECTION('ref_axis',(1.,0.,0.));
#17469=DIRECTION('',(-0.447213595499958,0.894427190999916,-5.47678698264203E-17));
#17470=DIRECTION('center_axis',(0.,-1.,0.));
#17471=DIRECTION('ref_axis',(1.,0.,0.));
#17472=DIRECTION('center_axis',(0.,1.,0.));
#17473=DIRECTION('ref_axis',(1.,0.,0.));
#17474=DIRECTION('',(0.,1.,0.));
#17475=DIRECTION('center_axis',(0.,1.,0.));
#17476=DIRECTION('ref_axis',(1.,0.,0.));
#17477=DIRECTION('center_axis',(0.,-1.,0.));
#17478=DIRECTION('ref_axis',(1.,0.,0.));
#17479=DIRECTION('',(-0.707106781186547,0.707106781186548,-8.65956056235493E-17));
#17480=DIRECTION('center_axis',(0.,-1.,0.));
#17481=DIRECTION('ref_axis',(0.,0.,-1.));
#17482=DIRECTION('center_axis',(0.866025403784439,0.,-0.5));
#17483=DIRECTION('ref_axis',(0.5,0.,0.866025403784439));
#17484=DIRECTION('',(-0.5,0.,-0.866025403784439));
#17485=DIRECTION('',(0.,-1.,0.));
#17486=DIRECTION('',(0.5,0.,0.866025403784439));
#17487=DIRECTION('',(0.,-1.,0.));
#17488=DIRECTION('center_axis',(1.20185167898973E-16,0.,-1.));
#17489=DIRECTION('ref_axis',(1.,0.,1.20185167898973E-16));
#17490=DIRECTION('',(-1.,0.,-1.20185167898973E-16));
#17491=DIRECTION('',(0.,-1.,0.));
#17492=DIRECTION('',(1.,0.,1.20185167898973E-16));
#17493=DIRECTION('center_axis',(-0.866025403784439,0.,-0.5));
#17494=DIRECTION('ref_axis',(0.5,0.,-0.866025403784439));
#17495=DIRECTION('',(-0.5,0.,0.866025403784439));
#17496=DIRECTION('',(0.,-1.,0.));
#17497=DIRECTION('',(0.5,0.,-0.866025403784439));
#17498=DIRECTION('center_axis',(-0.866025403784439,0.,0.5));
#17499=DIRECTION('ref_axis',(-0.5,0.,-0.866025403784439));
#17500=DIRECTION('',(0.5,0.,0.866025403784439));
#17501=DIRECTION('',(0.,-1.,0.));
#17502=DIRECTION('',(-0.5,0.,-0.866025403784439));
#17503=DIRECTION('center_axis',(-2.40370335797945E-16,0.,1.));
#17504=DIRECTION('ref_axis',(-1.,0.,-2.40370335797945E-16));
#17505=DIRECTION('',(1.,0.,2.40370335797945E-16));
#17506=DIRECTION('',(0.,-1.,0.));
#17507=DIRECTION('',(-1.,0.,-2.40370335797945E-16));
#17508=DIRECTION('center_axis',(0.866025403784439,0.,0.5));
#17509=DIRECTION('ref_axis',(-0.5,0.,0.866025403784439));
#17510=DIRECTION('',(0.5,0.,-0.866025403784439));
#17511=DIRECTION('',(-0.5,0.,0.866025403784439));
#17512=DIRECTION('center_axis',(0.,1.,0.));
#17513=DIRECTION('ref_axis',(1.,0.,0.));
#17514=DIRECTION('center_axis',(0.,-1.,0.));
#17515=DIRECTION('ref_axis',(0.,0.,-1.));
#23612=CARTESIAN_POINT('',(0.,0.,0.));
#23613=CARTESIAN_POINT('Origin',(0.375,0.5,0.));
#23614=CARTESIAN_POINT('',(-0.375,0.5,-4.59242549680257E-17));
#23615=CARTESIAN_POINT('Origin',(0.,0.5,0.));
#23616=CARTESIAN_POINT('Origin',(0.,0.475,0.));
#23617=CARTESIAN_POINT('',(-0.425,0.45,-5.20474889637625E-17));
#23618=CARTESIAN_POINT('Origin',(0.,0.45,0.));
#23619=CARTESIAN_POINT('',(-0.4,0.475,-4.89858719658941E-17));
#23620=CARTESIAN_POINT('Origin',(0.,0.24,0.));
#23621=CARTESIAN_POINT('',(-0.425,0.0299999999999998,-5.20474889637625E-17));
#23622=CARTESIAN_POINT('Origin',(0.,0.0299999999999998,0.));
#23623=CARTESIAN_POINT('',(-0.425,0.24,-5.20474889637625E-17));
#23624=CARTESIAN_POINT('Origin',(0.,0.0150000000000001,0.));
#23625=CARTESIAN_POINT('',(-0.395,4.85722573273506E-17,-4.83735485663204E-17));
#23626=CARTESIAN_POINT('Origin',(0.,0.,0.));
#23627=CARTESIAN_POINT('',(-0.41,0.0150000000000001,-5.02105187650415E-17));
#23628=CARTESIAN_POINT('Origin',(0.27,0.,0.));
#23629=CARTESIAN_POINT('',(-0.27,0.,-3.30654635769785E-17));
#23630=CARTESIAN_POINT('Origin',(0.,0.,0.));
#23631=CARTESIAN_POINT('Origin',(0.,-0.02,0.));
#23632=CARTESIAN_POINT('',(-0.24505,-0.0498999999999999,3.00099698131059E-17));
#23633=CARTESIAN_POINT('Origin',(0.,-0.0498999999999999,0.));
#23634=CARTESIAN_POINT('',(-0.26,-0.02,-3.18408167778312E-17));
#23635=CARTESIAN_POINT('Origin',(0.,-0.995,0.));
#23636=CARTESIAN_POINT('',(-0.24505,-1.95495,3.00099698131059E-17));
#23637=CARTESIAN_POINT('Origin',(0.,-1.95495,0.));
#23638=CARTESIAN_POINT('',(-0.24505,-0.995,-3.00099698131059E-17));
#23639=CARTESIAN_POINT('Origin',(0.,-1.975,0.));
#23640=CARTESIAN_POINT('',(-0.2,-2.,-2.44929359829471E-17));
#23641=CARTESIAN_POINT('Origin',(0.,-2.,0.));
#23642=CARTESIAN_POINT('',(-0.225,-1.975,-2.75545529808154E-17));
#23643=CARTESIAN_POINT('Origin',(0.,-2.,0.));
#23644=CARTESIAN_POINT('Origin',(0.115470053837925,-0.5,-0.2));
#23645=CARTESIAN_POINT('',(0.23094010767585,-0.5,0.));
#23646=CARTESIAN_POINT('',(0.115470053837925,-0.5,-0.2));
#23647=CARTESIAN_POINT('',(0.23094010767585,-0.5,0.));
#23648=CARTESIAN_POINT('',(0.115470053837925,-0.8,-0.2));
#23649=CARTESIAN_POINT('',(0.115470053837925,-0.5,-0.2));
#23650=CARTESIAN_POINT('',(0.23094010767585,-0.8,0.));
#23651=CARTESIAN_POINT('',(0.23094010767585,-0.8,0.));
#23652=CARTESIAN_POINT('',(0.23094010767585,-0.5,0.));
#23653=CARTESIAN_POINT('Origin',(-0.115470053837925,-0.5,-0.2));
#23654=CARTESIAN_POINT('',(-0.115470053837925,-0.5,-0.2));
#23655=CARTESIAN_POINT('',(0.115470053837925,-0.5,-0.2));
#23656=CARTESIAN_POINT('',(-0.115470053837925,-0.8,-0.2));
#23657=CARTESIAN_POINT('',(-0.115470053837925,-0.5,-0.2));
#23658=CARTESIAN_POINT('',(0.115470053837925,-0.8,-0.2));
#23659=CARTESIAN_POINT('Origin',(-0.23094010767585,-0.5,-2.77555756156289E-17));
#23660=CARTESIAN_POINT('',(-0.23094010767585,-0.5,-2.82820063659975E-17));
#23661=CARTESIAN_POINT('',(-0.115470053837925,-0.5,-0.2));
#23662=CARTESIAN_POINT('',(-0.23094010767585,-0.8,-2.77555756156289E-17));
#23663=CARTESIAN_POINT('',(-0.23094010767585,-0.5,-2.82820063659975E-17));
#23664=CARTESIAN_POINT('',(-0.115470053837925,-0.8,-0.2));
#23665=CARTESIAN_POINT('Origin',(-0.115470053837925,-0.5,0.2));
#23666=CARTESIAN_POINT('',(-0.115470053837925,-0.5,0.2));
#23667=CARTESIAN_POINT('',(-0.23094010767585,-0.5,-2.82820063659975E-17));
#23668=CARTESIAN_POINT('',(-0.115470053837925,-0.8,0.2));
#23669=CARTESIAN_POINT('',(-0.115470053837925,-0.5,0.2));
#23670=CARTESIAN_POINT('',(-0.23094010767585,-0.8,-2.82820063659975E-17));
#23671=CARTESIAN_POINT('Origin',(0.115470053837925,-0.5,0.2));
#23672=CARTESIAN_POINT('',(0.115470053837925,-0.5,0.2));
#23673=CARTESIAN_POINT('',(-0.115470053837925,-0.5,0.2));
#23674=CARTESIAN_POINT('',(0.115470053837925,-0.8,0.2));
#23675=CARTESIAN_POINT('',(0.115470053837925,-0.5,0.2));
#23676=CARTESIAN_POINT('',(-0.115470053837925,-0.8,0.2));
#23677=CARTESIAN_POINT('Origin',(0.23094010767585,-0.5,0.));
#23678=CARTESIAN_POINT('',(0.115470053837925,-0.5,0.2));
#23679=CARTESIAN_POINT('',(0.115470053837925,-0.8,0.2));
#23680=CARTESIAN_POINT('Origin',(0.,-0.5,0.));
#23681=CARTESIAN_POINT('Origin',(0.,-0.8,0.));
#33917=UNCERTAINTY_MEASURE_WITH_UNIT(LENGTH_MEASURE(0.001),#33982,
'DISTANCE_ACCURACY_VALUE',
'Maximum model space distance between geometric entities at asserted c
onnectivities');
#33929=UNCERTAINTY_MEASURE_WITH_UNIT(LENGTH_MEASURE(0.001),#33982,
'DISTANCE_ACCURACY_VALUE',
'Maximum model space distance between geometric entities at asserted c
onnectivities');
#33969=(
GEOMETRIC_REPRESENTATION_CONTEXT(3)
GLOBAL_UNCERTAINTY_ASSIGNED_CONTEXT((#33917))
GLOBAL_UNIT_ASSIGNED_CONTEXT((#33982,#33984,#33985))
REPRESENTATION_CONTEXT('','3D')
);
#33981=(
GEOMETRIC_REPRESENTATION_CONTEXT(3)
GLOBAL_UNCERTAINTY_ASSIGNED_CONTEXT((#33929))
GLOBAL_UNIT_ASSIGNED_CONTEXT((#33982,#33984,#33985))
REPRESENTATION_CONTEXT('','3D')
);
#33982=(
LENGTH_UNIT()
NAMED_UNIT(*)
SI_UNIT(.CENTI.,.METRE.)
);
#33984=(
NAMED_UNIT(*)
PLANE_ANGLE_UNIT()
SI_UNIT($,.RADIAN.)
);
#33985=(
NAMED_UNIT(*)
SI_UNIT($,.STERADIAN.)
SOLID_ANGLE_UNIT()
);
#34025=SHAPE_DEFINITION_REPRESENTATION(#34089,#34221);
#34089=PRODUCT_DEFINITION_SHAPE('',$,#34273);
#34221=SHAPE_REPRESENTATION('',(#14499),#33969);
#34233=PRODUCT_DEFINITION_CONTEXT('part definition',#34388,'design');
#34273=PRODUCT_DEFINITION('Cap Screw - M5x20','Cap Screw - M5x20',#34324,
#34233);
#34324=PRODUCT_DEFINITION_FORMATION('',$,#34429);
#34388=APPLICATION_CONTEXT(
'Core Data for Automotive Mechanical Design Process');
#34389=PRODUCT_CONTEXT('part definition',#34388,'mechanical');
#34429=PRODUCT('Cap Screw - M5x20','Cap Screw - M5x20',
'Cap Screw - M5x20',(#34389));
#34518=COLOUR_RGB('Black',0.12,0.14,0.17);
#34519=FILL_AREA_STYLE_COLOUR('',#34518);
#34520=FILL_AREA_STYLE('',(#34519));
#34521=SURFACE_STYLE_FILL_AREA(#34520);
#34522=SURFACE_SIDE_STYLE('',(#34521));
#34523=SURFACE_STYLE_USAGE(.BOTH.,#34522);
#34524=PRESENTATION_STYLE_ASSIGNMENT((#34523));
ENDSEC;
END-ISO-10303-21;
